ISO-10303-21;
HEADER;
/* Generated by software containing ST-Developer
 * from STEP Tools, Inc. (www.steptools.com) 
 */

FILE_DESCRIPTION(
/* description */ ('Flywheel Crank-Slider'),
/* implementation_level */ '2;1');

FILE_NAME(
/* name */ 'Rod bearing retainer (1).step',
/* time_stamp */ '2026-10-28T03:23:13-07:00',
/* author */ (''),
/* organization */ (''),
/* preprocessor_version */ 'ST-DEVELOPER v20.2',
/* originating_system */ 'Autodesk Translation Framework v15.17.0.0',
/* authorisation */ '');

FILE_SCHEMA (('AUTOMOTIVE_DESIGN { 1 0 10303 214 3 1 1 }'));
ENDSEC;

DATA;
#10=MECHANICAL_DESIGN_GEOMETRIC_PRESENTATION_REPRESENTATION('',(#703),#17322);
#598=SHAPE_REPRESENTATION_RELATIONSHIP('SRR','None',#17597,#650);
#650=ADVANCED_BREP_SHAPE_REPRESENTATION('',(#760),#17301);
#703=STYLED_ITEM('',(#17931),#760);
#760=MANIFOLD_SOLID_BREP('Body1',#9085);
#937=FACE_BOUND('',#2380,.T.);
#938=FACE_BOUND('',#2382,.T.);
#1236=PLANE('',#10373);
#1237=PLANE('',#10374);
#1690=FACE_OUTER_BOUND('',#2377,.T.);
#1691=FACE_OUTER_BOUND('',#2378,.T.);
#1692=FACE_OUTER_BOUND('',#2379,.T.);
#1693=FACE_OUTER_BOUND('',#2381,.T.);
#2377=EDGE_LOOP('',(#7662,#7663,#7664,#7665));
#2378=EDGE_LOOP('',(#7666,#7667,#7668,#7669));
#2379=EDGE_LOOP('',(#7670));
#2380=EDGE_LOOP('',(#7671));
#2381=EDGE_LOOP('',(#7672));
#2382=EDGE_LOOP('',(#7673));
#3080=LINE('',#16008,#3691);
#3081=LINE('',#16014,#3692);
#3691=VECTOR('',#12662,1.1);
#3692=VECTOR('',#12669,2.);
#4108=CIRCLE('',#10368,1.1);
#4109=CIRCLE('',#10369,1.1);
#4110=CIRCLE('',#10371,2.);
#4111=CIRCLE('',#10372,2.);
#4787=VERTEX_POINT('',#16005);
#4788=VERTEX_POINT('',#16007);
#4789=VERTEX_POINT('',#16011);
#4790=VERTEX_POINT('',#16013);
#5788=EDGE_CURVE('',#4787,#4787,#4108,.T.);
#5789=EDGE_CURVE('',#4787,#4788,#3080,.T.);
#5790=EDGE_CURVE('',#4788,#4788,#4109,.T.);
#5791=EDGE_CURVE('',#4789,#4789,#4110,.T.);
#5792=EDGE_CURVE('',#4789,#4790,#3081,.T.);
#5793=EDGE_CURVE('',#4790,#4790,#4111,.T.);
#7662=ORIENTED_EDGE('',*,*,#5788,.F.);
#7663=ORIENTED_EDGE('',*,*,#5789,.T.);
#7664=ORIENTED_EDGE('',*,*,#5790,.T.);
#7665=ORIENTED_EDGE('',*,*,#5789,.F.);
#7666=ORIENTED_EDGE('',*,*,#5791,.F.);
#7667=ORIENTED_EDGE('',*,*,#5792,.T.);
#7668=ORIENTED_EDGE('',*,*,#5793,.T.);
#7669=ORIENTED_EDGE('',*,*,#5792,.F.);
#7670=ORIENTED_EDGE('',*,*,#5791,.T.);
#7671=ORIENTED_EDGE('',*,*,#5788,.T.);
#7672=ORIENTED_EDGE('',*,*,#5793,.F.);
#7673=ORIENTED_EDGE('',*,*,#5790,.F.);
#8455=CYLINDRICAL_SURFACE('',#10367,1.1);
#8456=CYLINDRICAL_SURFACE('',#10370,2.);
#8881=ADVANCED_FACE('',(#1690),#8455,.F.);
#8882=ADVANCED_FACE('',(#1691),#8456,.T.);
#8883=ADVANCED_FACE('',(#1692,#937),#1236,.T.);
#8884=ADVANCED_FACE('',(#1693,#938),#1237,.F.);
#9085=CLOSED_SHELL('',(#8881,#8882,#8883,#8884));
#10366=AXIS2_PLACEMENT_3D('',#16003,#12656,#12657);
#10367=AXIS2_PLACEMENT_3D('',#16004,#12658,#12659);
#10368=AXIS2_PLACEMENT_3D('',#16006,#12660,#12661);
#10369=AXIS2_PLACEMENT_3D('',#16009,#12663,#12664);
#10370=AXIS2_PLACEMENT_3D('',#16010,#12665,#12666);
#10371=AXIS2_PLACEMENT_3D('',#16012,#12667,#12668);
#10372=AXIS2_PLACEMENT_3D('',#16015,#12670,#12671);
#10373=AXIS2_PLACEMENT_3D('',#16016,#12672,#12673);
#10374=AXIS2_PLACEMENT_3D('',#16017,#12674,#12675);
#12656=DIRECTION('axis',(0.,0.,1.));
#12657=DIRECTION('refdir',(1.,0.,0.));
#12658=DIRECTION('center_axis',(0.,1.,0.));
#12659=DIRECTION('ref_axis',(1.,0.,0.));
#12660=DIRECTION('center_axis',(0.,-1.,0.));
#12661=DIRECTION('ref_axis',(1.,0.,0.));
#12662=DIRECTION('',(0.,-1.,0.));
#12663=DIRECTION('center_axis',(0.,-1.,0.));
#12664=DIRECTION('ref_axis',(1.,0.,0.));
#12665=DIRECTION('center_axis',(0.,1.,0.));
#12666=DIRECTION('ref_axis',(1.,0.,0.));
#12667=DIRECTION('center_axis',(0.,1.,0.));
#12668=DIRECTION('ref_axis',(1.,0.,0.));
#12669=DIRECTION('',(0.,-1.,0.));
#12670=DIRECTION('center_axis',(0.,1.,0.));
#12671=DIRECTION('ref_axis',(1.,0.,0.));
#12672=DIRECTION('center_axis',(0.,1.,0.));
#12673=DIRECTION('ref_axis',(1.,0.,0.));
#12674=DIRECTION('center_axis',(0.,1.,0.));
#12675=DIRECTION('ref_axis',(1.,0.,0.));
#16003=CARTESIAN_POINT('',(0.,0.,0.));
#16004=CARTESIAN_POINT('Origin',(2.,3.4,10.));
#16005=CARTESIAN_POINT('',(0.9,3.6,10.));
#16006=CARTESIAN_POINT('Origin',(2.,3.6,10.));
#16007=CARTESIAN_POINT('',(0.9,3.4,10.));
#16008=CARTESIAN_POINT('',(0.9,3.4,10.));
#16009=CARTESIAN_POINT('Origin',(2.,3.4,10.));
#16010=CARTESIAN_POINT('Origin',(2.,3.4,10.));
#16011=CARTESIAN_POINT('',(0.,3.6,10.));
#16012=CARTESIAN_POINT('Origin',(2.,3.6,10.));
#16013=CARTESIAN_POINT('',(0.,3.4,10.));
#16014=CARTESIAN_POINT('',(0.,3.4,10.));
#16015=CARTESIAN_POINT('Origin',(2.,3.4,10.));
#16016=CARTESIAN_POINT('Origin',(2.,3.6,10.));
#16017=CARTESIAN_POINT('Origin',(2.,3.4,10.));
#17240=UNCERTAINTY_MEASURE_WITH_UNIT(LENGTH_MEASURE(0.001),#17323,
'DISTANCE_ACCURACY_VALUE',
'Maximum model space distance between geometric entities at asserted c
onnectivities');
#17261=UNCERTAINTY_MEASURE_WITH_UNIT(LENGTH_MEASURE(0.001),#17323,
'DISTANCE_ACCURACY_VALUE',
'Maximum model space distance between geometric entities at asserted c
onnectivities');
#17301=(
GEOMETRIC_REPRESENTATION_CONTEXT(3)
GLOBAL_UNCERTAINTY_ASSIGNED_CONTEXT((#17240))
GLOBAL_UNIT_ASSIGNED_CONTEXT((#17323,#17325,#17326))
REPRESENTATION_CONTEXT('','3D')
);
#17322=(
GEOMETRIC_REPRESENTATION_CONTEXT(3)
GLOBAL_UNCERTAINTY_ASSIGNED_CONTEXT((#17261))
GLOBAL_UNIT_ASSIGNED_CONTEXT((#17323,#17325,#17326))
REPRESENTATION_CONTEXT('','3D')
);
#17323=(
LENGTH_UNIT()
NAMED_UNIT(*)
SI_UNIT(.CENTI.,.METRE.)
);
#17325=(
NAMED_UNIT(*)
PLANE_ANGLE_UNIT()
SI_UNIT($,.RADIAN.)
);
#17326=(
NAMED_UNIT(*)
SI_UNIT($,.STERADIAN.)
SOLID_ANGLE_UNIT()
);
#17366=SHAPE_DEFINITION_REPRESENTATION(#17428,#17597);
#17428=PRODUCT_DEFINITION_SHAPE('',$,#17658);
#17597=SHAPE_REPRESENTATION('',(#10366),#17301);
#17618=PRODUCT_DEFINITION_CONTEXT('part definition',#17800,'design');
#17658=PRODUCT_DEFINITION('Rod bearing retainer (1)',
'Rod bearing retainer (1)',#17718,#17618);
#17718=PRODUCT_DEFINITION_FORMATION('',$,#17841);
#17800=APPLICATION_CONTEXT(
'Core Data for Automotive Mechanical Design Process');
#17801=PRODUCT_CONTEXT('part definition',#17800,'mechanical');
#17841=PRODUCT('Rod bearing retainer (1)','Rod bearing retainer (1)',
'Rod bearing retainer (1)',(#17801));
#17925=COLOUR_RGB('Grey',0.48,0.52,0.57);
#17926=FILL_AREA_STYLE_COLOUR('',#17925);
#17927=FILL_AREA_STYLE('',(#17926));
#17928=SURFACE_STYLE_FILL_AREA(#17927);
#17929=SURFACE_SIDE_STYLE('',(#17928));
#17930=SURFACE_STYLE_USAGE(.BOTH.,#17929);
#17931=PRESENTATION_STYLE_ASSIGNMENT((#17930));
ENDSEC;
END-ISO-10303-21;
